ISO-10303-21;
HEADER;
FILE_DESCRIPTION (('STEP AP214'),
    '1' );
FILE_NAME ('Latch Lever Guide.step',
    '2026-10-06T13:23:30',
    ( '' ),
    ( '' ),
    'SwSTEP 2.0',
    'SolidWorks 2020',
    '' );
FILE_SCHEMA (( 'AUTOMOTIVE_DESIGN' ));
ENDSEC;

DATA;
#72=( NAMED_UNIT ( * ) PLANE_ANGLE_UNIT ( ) SI_UNIT ( $, .RADIAN. ) );
#144=CARTESIAN_POINT ( 'NONE',  ( 9.683200060759999062, -20.50000000000000000, -149.3052959529999839 ) ) ;
#260=ORIENTED_EDGE ( 'NONE', *, *, #13143, .F. ) ;
#296=SHAPE_REPRESENTATION_RELATIONSHIP ( 'NONE' , 'NONE' ,  #13440, #10650 ) ;
#357=FACE_OUTER_BOUND ( 'NONE', #9688, .T. ) ;
#434=DIRECTION ( 'NONE',  ( -1.000000000000000000, 0.000000000000000000, 0.000000000000000000 ) ) ;
#649=ORIENTED_EDGE ( 'NONE', *, *, #19647, .F. ) ;
#729=CIRCLE ( 'NONE', #20480, 1.000000000000000888 ) ;
#771=VECTOR ( 'NONE', #1393, 1000.000000000000000 ) ;
#835=CARTESIAN_POINT ( 'NONE',  ( 13.68320006080000084, -19.50000000000000000, -148.5552959529999839 ) ) ;
#856=CARTESIAN_POINT ( 'NONE',  ( 7.683200060759999950, -19.50000000000000000, -148.5552959529999839 ) ) ;
#862=VECTOR ( 'NONE', #11868, 1000.000000000000000 ) ;
#881=EDGE_CURVE ( 'NONE', #17860, #7320, #15289, .T. ) ;
#988=APPLICATION_CONTEXT ( 'automotive_design' ) ;
#1021=DIRECTION ( 'NONE',  ( 0.000000000000000000, -1.000000000000000000, 0.000000000000000000 ) ) ;
#1057=CYLINDRICAL_SURFACE ( 'NONE', #12060, 1.000000000000000888 ) ;
#1119=EDGE_CURVE ( 'NONE', #11281, #5200, #3287, .T. ) ;
#1161=DIRECTION ( 'NONE',  ( 1.000000000000000000, 0.000000000000000000, 0.000000000000000000 ) ) ;
#1197=ORIENTED_EDGE ( 'NONE', *, *, #22760, .F. ) ;
#1212=ORIENTED_EDGE ( 'NONE', *, *, #5354, .T. ) ;
#1347=VERTEX_POINT ( 'NONE', #15293 ) ;
#1365=DIRECTION ( 'NONE',  ( 1.000000000000000000, 3.994014904670000134E-29, -2.423380700840000070E-27 ) ) ;
#1393=DIRECTION ( 'NONE',  ( 1.000000000000000000, 0.000000000000000000, 0.000000000000000000 ) ) ;
#1466=AXIS2_PLACEMENT_3D ( 'NONE', #2201, #1978, #9551 ) ;
#1501=PRODUCT_CONTEXT ( 'NONE', #3407, 'mechanical' ) ;
#1661=DIRECTION ( 'NONE',  ( 0.000000000000000000, -4.148443855749999753E-27, -1.000000000000000000 ) ) ;
#1798=LINE ( 'NONE', #11048, #11607 ) ;
#1816=ORIENTED_EDGE ( 'NONE', *, *, #23431, .T. ) ;
#1978=DIRECTION ( 'NONE',  ( -1.000000000000000000, -3.994014904670000134E-29, 2.423380700840000070E-27 ) ) ;
#1990=CARTESIAN_POINT ( 'NONE',  ( 7.683200060759999950, -19.50000000000000000, -138.5552959529999839 ) ) ;
#2067=DIRECTION ( 'NONE',  ( 1.000000000000000000, 0.000000000000000000, 0.000000000000000000 ) ) ;
#2201=CARTESIAN_POINT ( 'NONE',  ( 7.683200060759999950, -19.50000000000000000, -148.5552959529999839 ) ) ;
#2249=CARTESIAN_POINT ( 'NONE',  ( 13.68320006080000084, -21.50000000000000000, -138.5552959529999839 ) ) ;
#2292=AXIS2_PLACEMENT_3D ( 'NONE', #17739, #21989, #19535 ) ;
#2325=FACE_OUTER_BOUND ( 'NONE', #5206, .T. ) ;
#2383=CARTESIAN_POINT ( 'NONE',  ( 13.68320006080000084, -19.50000000000000000, -138.5552959529999839 ) ) ;
#2447=VERTEX_POINT ( 'NONE', #1990 ) ;
#2463=ORIENTED_EDGE ( 'NONE', *, *, #23431, .F. ) ;
#2603=DIRECTION ( 'NONE',  ( 1.211690350419999855E-27, 2.765629237170000203E-27, -1.000000000000000000 ) ) ;
#2637=DIRECTION ( 'NONE',  ( 1.000000000000000000, 0.000000000000000000, 0.000000000000000000 ) ) ;
#2787=PLANE ( 'NONE',  #9299 ) ;
#2825=ORIENTED_EDGE ( 'NONE', *, *, #13893, .F. ) ;
#2829=EDGE_CURVE ( 'NONE', #17860, #14260, #14438, .T. ) ;
#2986=DIRECTION ( 'NONE',  ( 1.211690350419999855E-27, 2.765629237170000203E-27, -1.000000000000000000 ) ) ;
#3276=EDGE_LOOP ( 'NONE', ( #22085, #12399, #12926, #12667 ) ) ;
#3287=LINE ( 'NONE', #4960, #771 ) ;
#3391=PRESENTATION_STYLE_ASSIGNMENT (( #7083 ) ) ;
#3407=APPLICATION_CONTEXT ( 'automotive_design' ) ;
#3410=CARTESIAN_POINT ( 'NONE',  ( 10.68320006080000084, -20.50000000000000000, -148.5552959529999839 ) ) ;
#3468=COLOUR_RGB ( '', 0.72549020, 0.75294118, 0.79215686) ;
#3532=ORIENTED_EDGE ( 'NONE', *, *, #5354, .F. ) ;
#3665=CARTESIAN_POINT ( 'NONE',  ( 13.68320006080000084, -21.50000000000000000, -148.5552959529999839 ) ) ;
#3785=PRODUCT_DEFINITION_SHAPE ( 'NONE', 'NONE',  #19394 ) ;
#3833=DIRECTION ( 'NONE',  ( -1.000000000000000000, 0.000000000000000000, 0.000000000000000000 ) ) ;
#3949=CARTESIAN_POINT ( 'NONE',  ( 12.18320006080000084, -19.50000000000000000, -148.5552959529999839 ) ) ;
#3997=EDGE_CURVE ( 'NONE', #14626, #8533, #16513, .T. ) ;
#4241=AXIS2_PLACEMENT_3D ( 'NONE', #15009, #22389, #2067 ) ;
#4522=FACE_OUTER_BOUND ( 'NONE', #21064, .T. ) ;
#4566=( NAMED_UNIT ( * ) PLANE_ANGLE_UNIT ( ) SI_UNIT ( $, .RADIAN. ) );
#4590=CARTESIAN_POINT ( 'NONE',  ( 0.000000000000000000, 0.000000000000000000, 0.000000000000000000 ) ) ;
#4624=CARTESIAN_POINT ( 'NONE',  ( 7.683200060759999950, -21.50000000000000000, -143.5552959529999839 ) ) ;
#4960=CARTESIAN_POINT ( 'NONE',  ( 10.68320006080000084, -21.50000000000000000, -138.5552959529999839 ) ) ;
#4987=LINE ( 'NONE', #22962, #15681 ) ;
#5025=AXIS2_PLACEMENT_3D ( 'NONE', #4590, #17084, #1161 ) ;
#5092=VECTOR ( 'NONE', #5623, 1000.000000000000000 ) ;
#5096=EDGE_LOOP ( 'NONE', ( #11711, #1816, #10133, #16959, #23288 ) ) ;
#5200=VERTEX_POINT ( 'NONE', #2249 ) ;
#5206=EDGE_LOOP ( 'NONE', ( #11620, #3532, #11456, #23131, #12096 ) ) ;
#5268=EDGE_CURVE ( 'NONE', #11647, #17860, #729, .T. ) ;
#5313=DIRECTION ( 'NONE',  ( 1.211690350419999855E-27, 2.765629237170000203E-27, -1.000000000000000000 ) ) ;
#5354=EDGE_CURVE ( 'NONE', #22094, #11647, #9055, .T. ) ;
#5504=LINE ( 'NONE', #12751, #11442 ) ;
#5623=DIRECTION ( 'NONE',  ( 1.000000000000000000, 0.000000000000000000, 0.000000000000000000 ) ) ;
#5699=DIRECTION ( 'NONE',  ( -1.000000000000000000, 0.000000000000000000, 0.000000000000000000 ) ) ;
#5872=( NAMED_UNIT ( * ) SI_UNIT ( $, .STERADIAN. ) SOLID_ANGLE_UNIT ( ) );
#5984=DIRECTION ( 'NONE',  ( -1.000000000000000000, 0.000000000000000000, 0.000000000000000000 ) ) ;
#6026=ADVANCED_FACE ( 'NONE', ( #21809 ), #12740, .T. ) ;
#6052=AXIS2_PLACEMENT_3D ( 'NONE', #10943, #21276, #10308 ) ;
#6110=MECHANICAL_DESIGN_GEOMETRIC_PRESENTATION_REPRESENTATION('',(#21327),#9135);
#6124=AXIS2_PLACEMENT_3D ( 'NONE', #20055, #16371, #10753 ) ;
#6226=FACE_OUTER_BOUND ( 'NONE', #16747, .T. ) ;
#6339=DIRECTION ( 'NONE',  ( 0.000000000000000000, -1.000000000000000000, -2.765629237170000203E-27 ) ) ;
#6346=SURFACE_STYLE_FILL_AREA ( #15510 ) ;
#6375=ORIENTED_EDGE ( 'NONE', *, *, #22694, .F. ) ;
#6426=DIRECTION ( 'NONE',  ( 1.211690350419999855E-27, 2.765629237170000203E-27, -1.000000000000000000 ) ) ;
#6595=LINE ( 'NONE', #10390, #21157 ) ;
#6696=( LENGTH_UNIT ( ) NAMED_UNIT ( * ) SI_UNIT ( .MILLI., .METRE. ) );
#6722=FILL_AREA_STYLE_COLOUR ( '', #22134 ) ;
#7083=SURFACE_STYLE_USAGE ( .BOTH. , #19697 ) ;
#7231=LINE ( 'NONE', #19730, #15288 ) ;
#7283=ORIENTED_EDGE ( 'NONE', *, *, #15099, .T. ) ;
#7300=FACE_OUTER_BOUND ( 'NONE', #14242, .T. ) ;
#7320=VERTEX_POINT ( 'NONE', #18201 ) ;
#7353=ORIENTED_EDGE ( 'NONE', *, *, #22760, .T. ) ;
#7570=ADVANCED_FACE ( 'NONE', ( #16582 ), #18486, .T. ) ;
#7598=PLANE ( 'NONE',  #20222 ) ;
#7864=ORIENTED_EDGE ( 'NONE', *, *, #10533, .F. ) ;
#7874=CIRCLE ( 'NONE', #9769, 1.000000000000000888 ) ;
#7880=ORIENTED_EDGE ( 'NONE', *, *, #15499, .T. ) ;
#7966=AXIS2_PLACEMENT_3D ( 'NONE', #3665, #19964, #1661 ) ;
#8002=CARTESIAN_POINT ( 'NONE',  ( 7.683200060759999950, -19.50000000000000000, -148.5552959529999839 ) ) ;
#8085=DIRECTION ( 'NONE',  ( 3.994014902950000436E-29, -1.000000000000000000, 4.148443855749999753E-27 ) ) ;
#8114=CARTESIAN_POINT ( 'NONE',  ( 10.68320006080000084, -20.50000000000000000, -149.3052959529999839 ) ) ;
#8287=DIRECTION ( 'NONE',  ( -1.000000000000000000, 0.000000000000000000, 0.000000000000000000 ) ) ;
#8308=CARTESIAN_POINT ( 'NONE',  ( 13.68320006080000084, -21.50000000000000000, -148.5552959529999839 ) ) ;
#8533=VERTEX_POINT ( 'NONE', #23064 ) ;
#8549=CARTESIAN_POINT ( 'NONE',  ( 10.68320006080000084, -20.50000000000000000, -150.0552959529999839 ) ) ;
#8592=DIRECTION ( 'NONE',  ( -2.423380700840000070E-27, 0.000000000000000000, -1.000000000000000000 ) ) ;
#8642=FACE_OUTER_BOUND ( 'NONE', #5096, .T. ) ;
#8762=DIRECTION ( 'NONE',  ( 1.000000000000000000, 0.000000000000000000, 0.000000000000000000 ) ) ;
#8811=VERTEX_POINT ( 'NONE', #16576 ) ;
#8842=DIRECTION ( 'NONE',  ( 0.000000000000000000, 0.000000000000000000, 1.000000000000000000 ) ) ;
#8852=( NAMED_UNIT ( * ) SI_UNIT ( $, .STERADIAN. ) SOLID_ANGLE_UNIT ( ) );
#8885=ADVANCED_FACE ( 'NONE', ( #8642 ), #17948, .F. ) ;
#8926=LINE ( 'NONE', #3949, #15812 ) ;
#8966=PRODUCT_DEFINITION_CONTEXT ( 'detailed design', #988, 'design' ) ;
#8968=ORIENTED_EDGE ( 'NONE', *, *, #9339, .T. ) ;
#9055=CIRCLE ( 'NONE', #22378, 1.000000000000000888 ) ;
#9135=( GEOMETRIC_REPRESENTATION_CONTEXT ( 3 ) GLOBAL_UNCERTAINTY_ASSIGNED_CONTEXT ( ( #16130 ) ) GLOBAL_UNIT_ASSIGNED_CONTEXT ( ( #6696, #4566, #19193 ) ) REPRESENTATION_CONTEXT ( 'NONE', 'WORKASPACE' ) );
#9202=STYLED_ITEM ( 'NONE', ( #3391 ), #10650 ) ;
#9223=CARTESIAN_POINT ( 'NONE',  ( 9.183200060760000838, -19.50000000000000000, -148.5552959529999839 ) ) ;
#9240=ORIENTED_EDGE ( 'NONE', *, *, #19616, .F. ) ;
#9274=DIRECTION ( 'NONE',  ( 0.000000000000000000, 0.000000000000000000, -1.000000000000000000 ) ) ;
#9299=AXIS2_PLACEMENT_3D ( 'NONE', #9550, #22646, #6339 ) ;
#9339=EDGE_CURVE ( 'NONE', #14260, #23322, #14466, .T. ) ;
#9342=ORIENTED_EDGE ( 'NONE', *, *, #23303, .T. ) ;
#9425=ORIENTED_EDGE ( 'NONE', *, *, #17606, .F. ) ;
#9487=AXIS2_PLACEMENT_3D ( 'NONE', #14565, #1365, #8592 ) ;
#9536=ORIENTED_EDGE ( 'NONE', *, *, #881, .F. ) ;
#9550=CARTESIAN_POINT ( 'NONE',  ( 10.93320006080000084, -15.50000000000000000, -148.5552959529999839 ) ) ;
#9551=DIRECTION ( 'NONE',  ( -3.994014904670000134E-29, 1.000000000000000000, 0.000000000000000000 ) ) ;
#9673=VECTOR ( 'NONE', #19402, 1000.000000000000000 ) ;
#9688=EDGE_LOOP ( 'NONE', ( #13278, #7353 ) ) ;
#9711=CARTESIAN_POINT ( 'NONE',  ( 10.68320006080000084, -19.50000000000000000, -148.5552959529999839 ) ) ;
#9769=AXIS2_PLACEMENT_3D ( 'NONE', #15712, #6426, #2637 ) ;
#10133=ORIENTED_EDGE ( 'NONE', *, *, #2829, .T. ) ;
#10308=DIRECTION ( 'NONE',  ( 0.000000000000000000, -1.000000000000000000, -2.765629237170000203E-27 ) ) ;
#10390=CARTESIAN_POINT ( 'NONE',  ( 7.683200060759999950, -20.50000000000000000, -138.5552959529999839 ) ) ;
#10533=EDGE_CURVE ( 'NONE', #11647, #1347, #11222, .T. ) ;
#10646=ORIENTED_EDGE ( 'NONE', *, *, #881, .T. ) ;
#10650=ADVANCED_BREP_SHAPE_REPRESENTATION ( '', ( #11815, #5025 ), #21773 ) ;
#10689=EDGE_LOOP ( 'NONE', ( #9240, #9536, #2463, #19821, #11642 ) ) ;
#10753=DIRECTION ( 'NONE',  ( 0.000000000000000000, -1.000000000000000000, -2.765629237170000203E-27 ) ) ;
#10802=ADVANCED_FACE ( 'NONE', ( #7300 ), #21359, .T. ) ;
#10832=VECTOR ( 'NONE', #8842, 1000.000000000000000 ) ;
#10943=CARTESIAN_POINT ( 'NONE',  ( 10.93320006080000084, -15.50000000000000000, -138.5552959529999839 ) ) ;
#10985=PRODUCT ( 'Latch Lever Guide', 'Latch Lever Guide', '', ( #1501 ) ) ;
#11048=CARTESIAN_POINT ( 'NONE',  ( 10.68320006080000084, -19.50000000000000000, -138.5552959529999839 ) ) ;
#11104=UNCERTAINTY_MEASURE_WITH_UNIT (LENGTH_MEASURE( 1.000000000000000082E-05 ), #23502, 'distance_accuracy_value', 'NONE');
#11217=PLANE ( 'NONE',  #6124 ) ;
#11222=LINE ( 'NONE', #20647, #15590 ) ;
#11281=VERTEX_POINT ( 'NONE', #11937 ) ;
#11442=VECTOR ( 'NONE', #20024, 1000.000000000000000 ) ;
#11456=ORIENTED_EDGE ( 'NONE', *, *, #16152, .F. ) ;
#11472=MECHANICAL_DESIGN_GEOMETRIC_PRESENTATION_REPRESENTATION('',(#9202),#17956);
#11587=AXIS2_PLACEMENT_3D ( 'NONE', #8114, #20635, #5984 ) ;
#11607=VECTOR ( 'NONE', #5699, 1000.000000000000000 ) ;
#11620=ORIENTED_EDGE ( 'NONE', *, *, #5268, .F. ) ;
#11642=ORIENTED_EDGE ( 'NONE', *, *, #15099, .F. ) ;
#11647=VERTEX_POINT ( 'NONE', #20853 ) ;
#11674=AXIS2_PLACEMENT_3D ( 'NONE', #8549, #2986, #22727 ) ;
#11711=ORIENTED_EDGE ( 'NONE', *, *, #23303, .F. ) ;
#11815=MANIFOLD_SOLID_BREP ( 'lock_assembly.1\\deadbolt_assembly\\Product2.1\\dead bolt perpendicular.1\\PartBody', #17545 ) ;
#11868=DIRECTION ( 'NONE',  ( 0.000000000000000000, 0.000000000000000000, 1.000000000000000000 ) ) ;
#11937=CARTESIAN_POINT ( 'NONE',  ( 7.683200060759999950, -21.50000000000000000, -138.5552959529999839 ) ) ;
#12008=LINE ( 'NONE', #17490, #9673 ) ;
#12060=AXIS2_PLACEMENT_3D ( 'NONE', #22699, #2603, #8287 ) ;
#12096=ORIENTED_EDGE ( 'NONE', *, *, #2829, .F. ) ;
#12344=ADVANCED_FACE ( 'NONE', ( #14584 ), #11217, .F. ) ;
#12399=ORIENTED_EDGE ( 'NONE', *, *, #1119, .T. ) ;
#12419=( LENGTH_UNIT ( ) NAMED_UNIT ( * ) SI_UNIT ( .MILLI., .METRE. ) );
#12453=EDGE_LOOP ( 'NONE', ( #2825, #22687, #1212, #13156, #649 ) ) ;
#12667=ORIENTED_EDGE ( 'NONE', *, *, #17606, .T. ) ;
#12740=PLANE ( 'NONE',  #6052 ) ;
#12751=CARTESIAN_POINT ( 'NONE',  ( 13.68320006080000084, -21.50000000000000000, -143.5552959529999839 ) ) ;
#12926=ORIENTED_EDGE ( 'NONE', *, *, #13143, .T. ) ;
#13143=EDGE_CURVE ( 'NONE', #5200, #19847, #4987, .T. ) ;
#13156=ORIENTED_EDGE ( 'NONE', *, *, #10533, .T. ) ;
#13278=ORIENTED_EDGE ( 'NONE', *, *, #19647, .T. ) ;
#13440=SHAPE_REPRESENTATION ( 'Latch Lever Guide', ( #5025 ), #21773 ) ;
#13511=ORIENTED_EDGE ( 'NONE', *, *, #16368, .F. ) ;
#13721=CYLINDRICAL_SURFACE ( 'NONE', #11587, 1.000000000000000888 ) ;
#13847=SURFACE_STYLE_USAGE ( .BOTH. , #21228 ) ;
#13893=EDGE_CURVE ( 'NONE', #7320, #8811, #21918, .T. ) ;
#13983=( NAMED_UNIT ( * ) PLANE_ANGLE_UNIT ( ) SI_UNIT ( $, .RADIAN. ) );
#13999=VECTOR ( 'NONE', #20216, 1000.000000000000000 ) ;
#14099=LINE ( 'NONE', #23261, #10832 ) ;
#14242=EDGE_LOOP ( 'NONE', ( #6375, #8968, #7880, #260 ) ) ;
#14260=VERTEX_POINT ( 'NONE', #8308 ) ;
#14438=LINE ( 'NONE', #23366, #5092 ) ;
#14466=LINE ( 'NONE', #21734, #20118 ) ;
#14514=CIRCLE ( 'NONE', #4241, 1.000000000000000888 ) ;
#14565=CARTESIAN_POINT ( 'NONE',  ( 13.68320006080000084, -21.50000000000000000, -148.5552959529999839 ) ) ;
#14584=FACE_OUTER_BOUND ( 'NONE', #10689, .T. ) ;
#14626=VERTEX_POINT ( 'NONE', #8002 ) ;
#14725=CARTESIAN_POINT ( 'NONE',  ( 7.683200060759999950, -20.50000000000000000, -148.5552959529999839 ) ) ;
#14746=DIRECTION ( 'NONE',  ( -1.000000000000000000, 0.000000000000000000, -1.211690350419999855E-27 ) ) ;
#15009=CARTESIAN_POINT ( 'NONE',  ( 10.68320006080000084, -20.50000000000000000, -150.0552959529999839 ) ) ;
#15099=EDGE_CURVE ( 'NONE', #22094, #14626, #21865, .T. ) ;
#15288=VECTOR ( 'NONE', #8762, 1000.000000000000000 ) ;
#15289=CIRCLE ( 'NONE', #2292, 1.000000000000000888 ) ;
#15293=CARTESIAN_POINT ( 'NONE',  ( 11.68320006079999906, -20.50000000000000000, -150.0552959529999839 ) ) ;
#15323=CARTESIAN_POINT ( 'NONE',  ( 10.68320006080000084, -20.50000000000000000, -148.5552959529999839 ) ) ;
#15499=EDGE_CURVE ( 'NONE', #23322, #19847, #14099, .T. ) ;
#15510=FILL_AREA_STYLE ('',( #15747 ) ) ;
#15590=VECTOR ( 'NONE', #18496, 1000.000000000000000 ) ;
#15611=ORIENTED_EDGE ( 'NONE', *, *, #16368, .T. ) ;
#15681=VECTOR ( 'NONE', #21179, 1000.000000000000000 ) ;
#15691=LINE ( 'NONE', #4624, #862 ) ;
#15712=CARTESIAN_POINT ( 'NONE',  ( 10.68320006080000084, -20.50000000000000000, -148.5552959529999839 ) ) ;
#15747=FILL_AREA_STYLE_COLOUR ( '', #3468 ) ;
#15812=VECTOR ( 'NONE', #3833, 1000.000000000000000 ) ;
#15870=CIRCLE ( 'NONE', #11674, 1.000000000000000888 ) ;
#15885=FILL_AREA_STYLE ('',( #6722 ) ) ;
#16130=UNCERTAINTY_MEASURE_WITH_UNIT (LENGTH_MEASURE( 1.000000000000000082E-05 ), #6696, 'distance_accuracy_value', 'NONE');
#16132=SURFACE_STYLE_FILL_AREA ( #15885 ) ;
#16152=EDGE_CURVE ( 'NONE', #23322, #22094, #8926, .T. ) ;
#16368=EDGE_CURVE ( 'NONE', #14626, #2447, #12008, .T. ) ;
#16371=DIRECTION ( 'NONE',  ( -1.211690350419999855E-27, -2.765629237170000203E-27, 1.000000000000000000 ) ) ;
#16513=LINE ( 'NONE', #14725, #13999 ) ;
#16557=VECTOR ( 'NONE', #434, 1000.000000000000000 ) ;
#16576=CARTESIAN_POINT ( 'NONE',  ( 9.683200060759999062, -20.50000000000000000, -150.0552959529999839 ) ) ;
#16582=FACE_OUTER_BOUND ( 'NONE', #20274, .T. ) ;
#16747=EDGE_LOOP ( 'NONE', ( #7864, #21731, #10646, #17882, #1197 ) ) ;
#16945=ADVANCED_FACE ( 'NONE', ( #6226 ), #13721, .T. ) ;
#16959=ORIENTED_EDGE ( 'NONE', *, *, #22694, .T. ) ;
#17030=ADVANCED_FACE ( 'NONE', ( #2325 ), #2787, .F. ) ;
#17084=DIRECTION ( 'NONE',  ( 0.000000000000000000, 0.000000000000000000, 1.000000000000000000 ) ) ;
#17135=PLANE ( 'NONE',  #17334 ) ;
#17334=AXIS2_PLACEMENT_3D ( 'NONE', #856, #8085, #22610 ) ;
#17452=DIRECTION ( 'NONE',  ( 1.211690350419999855E-27, 2.765629237170000203E-27, -1.000000000000000000 ) ) ;
#17490=CARTESIAN_POINT ( 'NONE',  ( 7.683200060759999950, -19.50000000000000000, -143.5552959529999839 ) ) ;
#17545=CLOSED_SHELL ( 'NONE', ( #10802, #17030, #6026, #8885, #12344, #18661, #7570, #23107, #16945, #19980 ) ) ;
#17606=EDGE_CURVE ( 'NONE', #19847, #2447, #1798, .T. ) ;
#17701=CARTESIAN_POINT ( 'NONE',  ( 10.68320006080000084, -21.50000000000000000, -148.5552959529999839 ) ) ;
#17739=CARTESIAN_POINT ( 'NONE',  ( 10.68320006080000084, -20.50000000000000000, -148.5552959529999839 ) ) ;
#17860=VERTEX_POINT ( 'NONE', #17701 ) ;
#17882=ORIENTED_EDGE ( 'NONE', *, *, #13893, .T. ) ;
#17931=DIRECTION ( 'NONE',  ( 1.000000000000000000, 0.000000000000000000, 0.000000000000000000 ) ) ;
#17948=PLANE ( 'NONE',  #7966 ) ;
#17956=( GEOMETRIC_REPRESENTATION_CONTEXT ( 3 ) GLOBAL_UNCERTAINTY_ASSIGNED_CONTEXT ( ( #11104 ) ) GLOBAL_UNIT_ASSIGNED_CONTEXT ( ( #23502, #72, #5872 ) ) REPRESENTATION_CONTEXT ( 'NONE', 'WORKASPACE' ) );
#18165=EDGE_CURVE ( 'NONE', #2447, #11281, #6595, .T. ) ;
#18201=CARTESIAN_POINT ( 'NONE',  ( 9.683200060759999062, -20.50000000000000000, -148.5552959529999839 ) ) ;
#18486=PLANE ( 'NONE',  #1466 ) ;
#18496=DIRECTION ( 'NONE',  ( 0.000000000000000000, 0.000000000000000000, -1.000000000000000000 ) ) ;
#18661=ADVANCED_FACE ( 'NONE', ( #4522 ), #17135, .F. ) ;
#18988=ORIENTED_EDGE ( 'NONE', *, *, #18165, .F. ) ;
#19193=( NAMED_UNIT ( * ) SI_UNIT ( $, .STERADIAN. ) SOLID_ANGLE_UNIT ( ) );
#19374=FACE_OUTER_BOUND ( 'NONE', #12453, .T. ) ;
#19394=PRODUCT_DEFINITION ( 'UNKNOWN', '', #21420, #8966 ) ;
#19402=DIRECTION ( 'NONE',  ( 0.000000000000000000, 0.000000000000000000, 1.000000000000000000 ) ) ;
#19471=UNCERTAINTY_MEASURE_WITH_UNIT (LENGTH_MEASURE( 1.000000000000000082E-05 ), #12419, 'distance_accuracy_value', 'NONE');
#19535=DIRECTION ( 'NONE',  ( 1.000000000000000000, 0.000000000000000000, 0.000000000000000000 ) ) ;
#19616=EDGE_CURVE ( 'NONE', #7320, #22094, #7874, .T. ) ;
#19647=EDGE_CURVE ( 'NONE', #8811, #1347, #15870, .T. ) ;
#19697=SURFACE_SIDE_STYLE ('',( #16132 ) ) ;
#19730=CARTESIAN_POINT ( 'NONE',  ( 9.183200060760000838, -21.50000000000000000, -148.5552959529999839 ) ) ;
#19821=ORIENTED_EDGE ( 'NONE', *, *, #3997, .F. ) ;
#19823=DIRECTION ( 'NONE',  ( 0.000000000000000000, 1.000000000000000000, 0.000000000000000000 ) ) ;
#19847=VERTEX_POINT ( 'NONE', #2383 ) ;
#19964=DIRECTION ( 'NONE',  ( -3.994014902950000436E-29, 1.000000000000000000, -4.148443855749999753E-27 ) ) ;
#19980=ADVANCED_FACE ( 'NONE', ( #19374 ), #1057, .T. ) ;
#20024=DIRECTION ( 'NONE',  ( 0.000000000000000000, 0.000000000000000000, 1.000000000000000000 ) ) ;
#20055=CARTESIAN_POINT ( 'NONE',  ( 10.93320006080000084, -15.50000000000000000, -148.5552959529999839 ) ) ;
#20118=VECTOR ( 'NONE', #19823, 1000.000000000000000 ) ;
#20216=DIRECTION ( 'NONE',  ( 0.000000000000000000, -1.000000000000000000, 0.000000000000000000 ) ) ;
#20222=AXIS2_PLACEMENT_3D ( 'NONE', #20236, #22357, #14746 ) ;
#20236=CARTESIAN_POINT ( 'NONE',  ( 10.93320006080000084, -15.50000000000000000, -150.0552959529999839 ) ) ;
#20274=EDGE_LOOP ( 'NONE', ( #13511, #21660, #9342, #18988 ) ) ;
#20480=AXIS2_PLACEMENT_3D ( 'NONE', #15323, #17452, #23050 ) ;
#20635=DIRECTION ( 'NONE',  ( 1.211690350419999855E-27, 2.765629237170000203E-27, -1.000000000000000000 ) ) ;
#20647=CARTESIAN_POINT ( 'NONE',  ( 11.68320006079999906, -20.50000000000000000, -149.3052959529999839 ) ) ;
#20853=CARTESIAN_POINT ( 'NONE',  ( 11.68320006079999906, -20.50000000000000000, -148.5552959529999839 ) ) ;
#20871=PRESENTATION_STYLE_ASSIGNMENT (( #13847 ) ) ;
#21064=EDGE_LOOP ( 'NONE', ( #22189, #21506, #7283, #15611, #9425 ) ) ;
#21157=VECTOR ( 'NONE', #1021, 1000.000000000000000 ) ;
#21179=DIRECTION ( 'NONE',  ( 0.000000000000000000, 1.000000000000000000, 0.000000000000000000 ) ) ;
#21228=SURFACE_SIDE_STYLE ('',( #6346 ) ) ;
#21276=DIRECTION ( 'NONE',  ( -1.211690350419999855E-27, -2.765629237170000203E-27, 1.000000000000000000 ) ) ;
#21327=STYLED_ITEM ( 'NONE', ( #20871 ), #11815 ) ;
#21359=PLANE ( 'NONE',  #9487 ) ;
#21420=PRODUCT_DEFINITION_FORMATION_WITH_SPECIFIED_SOURCE ( 'ANY', '', #10985, .NOT_KNOWN. ) ;
#21506=ORIENTED_EDGE ( 'NONE', *, *, #16152, .T. ) ;
#21602=SHAPE_DEFINITION_REPRESENTATION ( #3785, #13440 ) ;
#21634=VECTOR ( 'NONE', #9274, 1000.000000000000000 ) ;
#21660=ORIENTED_EDGE ( 'NONE', *, *, #3997, .T. ) ;
#21731=ORIENTED_EDGE ( 'NONE', *, *, #5268, .T. ) ;
#21734=CARTESIAN_POINT ( 'NONE',  ( 13.68320006080000084, -20.50000000000000000, -148.5552959529999839 ) ) ;
#21773=( GEOMETRIC_REPRESENTATION_CONTEXT ( 3 ) GLOBAL_UNCERTAINTY_ASSIGNED_CONTEXT ( ( #19471 ) ) GLOBAL_UNIT_ASSIGNED_CONTEXT ( ( #12419, #13983, #8852 ) ) REPRESENTATION_CONTEXT ( 'NONE', 'WORKASPACE' ) );
#21809=FACE_OUTER_BOUND ( 'NONE', #3276, .T. ) ;
#21865=LINE ( 'NONE', #9223, #16557 ) ;
#21918=LINE ( 'NONE', #144, #21634 ) ;
#21989=DIRECTION ( 'NONE',  ( 1.211690350419999855E-27, 2.765629237170000203E-27, -1.000000000000000000 ) ) ;
#22085=ORIENTED_EDGE ( 'NONE', *, *, #18165, .T. ) ;
#22094=VERTEX_POINT ( 'NONE', #9711 ) ;
#22134=COLOUR_RGB ( '', 0.72549020, 0.75294118, 0.79215686) ;
#22189=ORIENTED_EDGE ( 'NONE', *, *, #15499, .F. ) ;
#22357=DIRECTION ( 'NONE',  ( 1.211690350419999855E-27, 2.765629237170000203E-27, -1.000000000000000000 ) ) ;
#22378=AXIS2_PLACEMENT_3D ( 'NONE', #3410, #5313, #17931 ) ;
#22389=DIRECTION ( 'NONE',  ( 1.211690350419999855E-27, 2.765629237170000203E-27, -1.000000000000000000 ) ) ;
#22610=DIRECTION ( 'NONE',  ( -1.000000000000000000, -3.994014902950000436E-29, 0.000000000000000000 ) ) ;
#22646=DIRECTION ( 'NONE',  ( -1.211690350419999855E-27, -2.765629237170000203E-27, 1.000000000000000000 ) ) ;
#22687=ORIENTED_EDGE ( 'NONE', *, *, #19616, .T. ) ;
#22694=EDGE_CURVE ( 'NONE', #14260, #5200, #5504, .T. ) ;
#22699=CARTESIAN_POINT ( 'NONE',  ( 10.68320006080000084, -20.50000000000000000, -149.3052959529999839 ) ) ;
#22727=DIRECTION ( 'NONE',  ( 1.000000000000000000, 0.000000000000000000, 0.000000000000000000 ) ) ;
#22760=EDGE_CURVE ( 'NONE', #1347, #8811, #14514, .T. ) ;
#22962=CARTESIAN_POINT ( 'NONE',  ( 13.68320006080000084, -20.50000000000000000, -138.5552959529999839 ) ) ;
#23050=DIRECTION ( 'NONE',  ( 1.000000000000000000, 0.000000000000000000, 0.000000000000000000 ) ) ;
#23064=CARTESIAN_POINT ( 'NONE',  ( 7.683200060759999950, -21.50000000000000000, -148.5552959529999839 ) ) ;
#23107=ADVANCED_FACE ( 'NONE', ( #357 ), #7598, .T. ) ;
#23131=ORIENTED_EDGE ( 'NONE', *, *, #9339, .F. ) ;
#23261=CARTESIAN_POINT ( 'NONE',  ( 13.68320006080000084, -19.50000000000000000, -143.5552959529999839 ) ) ;
#23288=ORIENTED_EDGE ( 'NONE', *, *, #1119, .F. ) ;
#23303=EDGE_CURVE ( 'NONE', #8533, #11281, #15691, .T. ) ;
#23322=VERTEX_POINT ( 'NONE', #835 ) ;
#23366=CARTESIAN_POINT ( 'NONE',  ( 12.18320006080000084, -21.50000000000000000, -148.5552959529999839 ) ) ;
#23431=EDGE_CURVE ( 'NONE', #8533, #17860, #7231, .T. ) ;
#23502=( LENGTH_UNIT ( ) NAMED_UNIT ( * ) SI_UNIT ( .MILLI., .METRE. ) );
ENDSEC;
END-ISO-10303-21;
